ISO-10303-21;
HEADER;
/* Generated by software containing ST-Developer
 * from STEP Tools, Inc. (www.steptools.com) 
 */

FILE_DESCRIPTION(
/* description */ ('Pallet stop with pneumatic fitting'),
/* implementation_level */ '2;1');

FILE_NAME(
/* name */ 'Hex Nut - M5.step',
/* time_stamp */ '2026-10-27T10:51:41-07:00',
/* author */ (''),
/* organization */ (''),
/* preprocessor_version */ 'ST-DEVELOPER v20.2',
/* originating_system */ 'Autodesk Translation Framework v15.17.0.0',
/* authorisation */ '');

FILE_SCHEMA (('AUTOMOTIVE_DESIGN { 1 0 10303 214 3 1 1 }'));
ENDSEC;

DATA;
#10=MECHANICAL_DESIGN_GEOMETRIC_PRESENTATION_REPRESENTATION('',(#381),#10265);
#11=(
BOUNDED_CURVE()
B_SPLINE_CURVE(2,(#9660,#9661,#9662),.UNSPECIFIED.,.F.,.F.)
B_SPLINE_CURVE_WITH_KNOTS((3,3),(0.140651836354967,0.670383167684795),
 .UNSPECIFIED.)
CURVE()
GEOMETRIC_REPRESENTATION_ITEM()
RATIONAL_B_SPLINE_CURVE((1.11602540378444,1.28867513459481,1.11602540378444))
REPRESENTATION_ITEM('')
);
#12=(
BOUNDED_CURVE()
B_SPLINE_CURVE(2,(#9664,#9665,#9666),.UNSPECIFIED.,.F.,.F.)
B_SPLINE_CURVE_WITH_KNOTS((3,3),(0.140651836354967,0.670383167684795),
 .UNSPECIFIED.)
CURVE()
GEOMETRIC_REPRESENTATION_ITEM()
RATIONAL_B_SPLINE_CURVE((1.11602540378444,1.28867513459481,1.11602540378444))
REPRESENTATION_ITEM('')
);
#13=(
BOUNDED_CURVE()
B_SPLINE_CURVE(2,(#9671,#9672,#9673),.UNSPECIFIED.,.F.,.F.)
B_SPLINE_CURVE_WITH_KNOTS((3,3),(0.140651836354967,0.670383167684795),
 .UNSPECIFIED.)
CURVE()
GEOMETRIC_REPRESENTATION_ITEM()
RATIONAL_B_SPLINE_CURVE((1.11602540378444,1.28867513459481,1.11602540378444))
REPRESENTATION_ITEM('')
);
#14=(
BOUNDED_CURVE()
B_SPLINE_CURVE(2,(#9675,#9676,#9677),.UNSPECIFIED.,.F.,.F.)
B_SPLINE_CURVE_WITH_KNOTS((3,3),(0.140651836354967,0.670383167684795),
 .UNSPECIFIED.)
CURVE()
GEOMETRIC_REPRESENTATION_ITEM()
RATIONAL_B_SPLINE_CURVE((1.11602540378444,1.28867513459481,1.11602540378444))
REPRESENTATION_ITEM('')
);
#15=(
BOUNDED_CURVE()
B_SPLINE_CURVE(2,(#9679,#9680,#9681),.UNSPECIFIED.,.F.,.F.)
B_SPLINE_CURVE_WITH_KNOTS((3,3),(0.140651836354967,0.670383167684795),
 .UNSPECIFIED.)
CURVE()
GEOMETRIC_REPRESENTATION_ITEM()
RATIONAL_B_SPLINE_CURVE((1.11602540378444,1.28867513459481,1.11602540378444))
REPRESENTATION_ITEM('')
);
#16=(
BOUNDED_CURVE()
B_SPLINE_CURVE(2,(#9682,#9683,#9684),.UNSPECIFIED.,.F.,.F.)
B_SPLINE_CURVE_WITH_KNOTS((3,3),(0.140651836354967,0.670383167684795),
 .UNSPECIFIED.)
CURVE()
GEOMETRIC_REPRESENTATION_ITEM()
RATIONAL_B_SPLINE_CURVE((1.11602540378444,1.28867513459481,1.11602540378444))
REPRESENTATION_ITEM('')
);
#17=(
BOUNDED_CURVE()
B_SPLINE_CURVE(2,(#9691,#9692,#9693),.UNSPECIFIED.,.F.,.F.)
B_SPLINE_CURVE_WITH_KNOTS((3,3),(0.140651836354967,0.670383167684795),
 .UNSPECIFIED.)
CURVE()
GEOMETRIC_REPRESENTATION_ITEM()
RATIONAL_B_SPLINE_CURVE((1.11602540378444,1.28867513459481,1.11602540378444))
REPRESENTATION_ITEM('')
);
#18=(
BOUNDED_CURVE()
B_SPLINE_CURVE(2,(#9695,#9696,#9697),.UNSPECIFIED.,.F.,.F.)
B_SPLINE_CURVE_WITH_KNOTS((3,3),(0.140651836354967,0.670383167684796),
 .UNSPECIFIED.)
CURVE()
GEOMETRIC_REPRESENTATION_ITEM()
RATIONAL_B_SPLINE_CURVE((1.11602540378444,1.28867513459481,1.11602540378444))
REPRESENTATION_ITEM('')
);
#19=(
BOUNDED_CURVE()
B_SPLINE_CURVE(2,(#9699,#9700,#9701),.UNSPECIFIED.,.F.,.F.)
B_SPLINE_CURVE_WITH_KNOTS((3,3),(0.140651836354967,0.670383167684795),
 .UNSPECIFIED.)
CURVE()
GEOMETRIC_REPRESENTATION_ITEM()
RATIONAL_B_SPLINE_CURVE((1.11602540378444,1.28867513459481,1.11602540378444))
REPRESENTATION_ITEM('')
);
#20=(
BOUNDED_CURVE()
B_SPLINE_CURVE(2,(#9703,#9704,#9705),.UNSPECIFIED.,.F.,.F.)
B_SPLINE_CURVE_WITH_KNOTS((3,3),(0.140651836354967,0.670383167684795),
 .UNSPECIFIED.)
CURVE()
GEOMETRIC_REPRESENTATION_ITEM()
RATIONAL_B_SPLINE_CURVE((1.11602540378444,1.28867513459482,1.11602540378444))
REPRESENTATION_ITEM('')
);
#21=(
BOUNDED_CURVE()
B_SPLINE_CURVE(2,(#9707,#9708,#9709),.UNSPECIFIED.,.F.,.F.)
B_SPLINE_CURVE_WITH_KNOTS((3,3),(0.140651836354967,0.670383167684795),
 .UNSPECIFIED.)
CURVE()
GEOMETRIC_REPRESENTATION_ITEM()
RATIONAL_B_SPLINE_CURVE((1.11602540378444,1.28867513459481,1.11602540378444))
REPRESENTATION_ITEM('')
);
#22=(
BOUNDED_CURVE()
B_SPLINE_CURVE(2,(#9710,#9711,#9712),.UNSPECIFIED.,.F.,.F.)
B_SPLINE_CURVE_WITH_KNOTS((3,3),(0.140651836354967,0.670383167684795),
 .UNSPECIFIED.)
CURVE()
GEOMETRIC_REPRESENTATION_ITEM()
RATIONAL_B_SPLINE_CURVE((1.11602540378444,1.28867513459481,1.11602540378444))
REPRESENTATION_ITEM('')
);
#30=CONICAL_SURFACE('',#5885,0.47094010767585,1.0471975511966);
#31=CONICAL_SURFACE('',#5887,0.47094010767585,1.0471975511966);
#317=SHAPE_REPRESENTATION_RELATIONSHIP('SRR','None',#10432,#349);
#349=ADVANCED_BREP_SHAPE_REPRESENTATION('',(#412),#10256);
#381=STYLED_ITEM('',(#10662),#412);
#412=MANIFOLD_SOLID_BREP('Body1',#5070);
#527=FACE_BOUND('',#1396,.T.);
#528=FACE_BOUND('',#1398,.T.);
#677=PLANE('',#5889);
#678=PLANE('',#5890);
#679=PLANE('',#5891);
#680=PLANE('',#5895);
#681=PLANE('',#5896);
#682=PLANE('',#5897);
#683=PLANE('',#5898);
#684=PLANE('',#5899);
#964=FACE_OUTER_BOUND('',#1386,.T.);
#965=FACE_OUTER_BOUND('',#1387,.T.);
#966=FACE_OUTER_BOUND('',#1388,.T.);
#967=FACE_OUTER_BOUND('',#1389,.T.);
#968=FACE_OUTER_BOUND('',#1390,.T.);
#969=FACE_OUTER_BOUND('',#1391,.T.);
#970=FACE_OUTER_BOUND('',#1392,.T.);
#971=FACE_OUTER_BOUND('',#1393,.T.);
#972=FACE_OUTER_BOUND('',#1394,.T.);
#973=FACE_OUTER_BOUND('',#1395,.T.);
#974=FACE_OUTER_BOUND('',#1397,.T.);
#1386=EDGE_LOOP('',(#4260,#4261,#4262,#4263,#4264,#4265,#4266,#4267,#4268));
#1387=EDGE_LOOP('',(#4269,#4270,#4271,#4272,#4273,#4274,#4275,#4276,#4277));
#1388=EDGE_LOOP('',(#4278,#4279,#4280,#4281));
#1389=EDGE_LOOP('',(#4282,#4283,#4284,#4285));
#1390=EDGE_LOOP('',(#4286,#4287,#4288,#4289));
#1391=EDGE_LOOP('',(#4290,#4291,#4292,#4293));
#1392=EDGE_LOOP('',(#4294,#4295,#4296,#4297));
#1393=EDGE_LOOP('',(#4298,#4299,#4300,#4301));
#1394=EDGE_LOOP('',(#4302,#4303,#4304,#4305));
#1395=EDGE_LOOP('',(#4306));
#1396=EDGE_LOOP('',(#4307));
#1397=EDGE_LOOP('',(#4308));
#1398=EDGE_LOOP('',(#4309));
#1715=LINE('',#9668,#2050);
#1716=LINE('',#9689,#2051);
#1717=LINE('',#9714,#2052);
#1718=LINE('',#9715,#2053);
#1719=LINE('',#9717,#2054);
#1720=LINE('',#9719,#2055);
#1721=LINE('',#9724,#2056);
#1722=LINE('',#9727,#2057);
#1723=LINE('',#9729,#2058);
#2050=VECTOR('',#7222,0.47094010767585);
#2051=VECTOR('',#7229,0.47094010767585);
#2052=VECTOR('',#7232,1.);
#2053=VECTOR('',#7233,1.);
#2054=VECTOR('',#7236,1.);
#2055=VECTOR('',#7239,1.);
#2056=VECTOR('',#7244,0.25);
#2057=VECTOR('',#7249,1.);
#2058=VECTOR('',#7252,1.);
#2353=CIRCLE('',#5886,0.38);
#2354=CIRCLE('',#5888,0.38);
#2355=CIRCLE('',#5893,0.2117);
#2356=CIRCLE('',#5894,0.2117);
#2687=VERTEX_POINT('',#9658);
#2688=VERTEX_POINT('',#9659);
#2689=VERTEX_POINT('',#9663);
#2690=VERTEX_POINT('',#9667);
#2691=VERTEX_POINT('',#9670);
#2692=VERTEX_POINT('',#9674);
#2693=VERTEX_POINT('',#9678);
#2694=VERTEX_POINT('',#9686);
#2695=VERTEX_POINT('',#9688);
#2696=VERTEX_POINT('',#9690);
#2697=VERTEX_POINT('',#9694);
#2698=VERTEX_POINT('',#9698);
#2699=VERTEX_POINT('',#9702);
#2700=VERTEX_POINT('',#9706);
#2701=VERTEX_POINT('',#9721);
#2702=VERTEX_POINT('',#9723);
#3229=EDGE_CURVE('',#2687,#2688,#11,.T.);
#3230=EDGE_CURVE('',#2689,#2687,#12,.T.);
#3231=EDGE_CURVE('',#2689,#2690,#1715,.T.);
#3232=EDGE_CURVE('',#2690,#2690,#2353,.T.);
#3233=EDGE_CURVE('',#2691,#2689,#13,.T.);
#3234=EDGE_CURVE('',#2692,#2691,#14,.T.);
#3235=EDGE_CURVE('',#2693,#2692,#15,.T.);
#3236=EDGE_CURVE('',#2688,#2693,#16,.T.);
#3237=EDGE_CURVE('',#2694,#2694,#2354,.T.);
#3238=EDGE_CURVE('',#2694,#2695,#1716,.T.);
#3239=EDGE_CURVE('',#2696,#2695,#17,.T.);
#3240=EDGE_CURVE('',#2697,#2696,#18,.T.);
#3241=EDGE_CURVE('',#2698,#2697,#19,.T.);
#3242=EDGE_CURVE('',#2699,#2698,#20,.T.);
#3243=EDGE_CURVE('',#2700,#2699,#21,.T.);
#3244=EDGE_CURVE('',#2695,#2700,#22,.T.);
#3245=EDGE_CURVE('',#2691,#2700,#1717,.T.);
#3246=EDGE_CURVE('',#2692,#2699,#1718,.T.);
#3247=EDGE_CURVE('',#2689,#2695,#1719,.T.);
#3248=EDGE_CURVE('',#2687,#2696,#1720,.T.);
#3249=EDGE_CURVE('',#2701,#2701,#2355,.F.);
#3250=EDGE_CURVE('',#2701,#2702,#1721,.T.);
#3251=EDGE_CURVE('',#2702,#2702,#2356,.F.);
#3252=EDGE_CURVE('',#2688,#2697,#1722,.T.);
#3253=EDGE_CURVE('',#2693,#2698,#1723,.T.);
#4260=ORIENTED_EDGE('',*,*,#3229,.F.);
#4261=ORIENTED_EDGE('',*,*,#3230,.F.);
#4262=ORIENTED_EDGE('',*,*,#3231,.T.);
#4263=ORIENTED_EDGE('',*,*,#3232,.F.);
#4264=ORIENTED_EDGE('',*,*,#3231,.F.);
#4265=ORIENTED_EDGE('',*,*,#3233,.F.);
#4266=ORIENTED_EDGE('',*,*,#3234,.F.);
#4267=ORIENTED_EDGE('',*,*,#3235,.F.);
#4268=ORIENTED_EDGE('',*,*,#3236,.F.);
#4269=ORIENTED_EDGE('',*,*,#3237,.F.);
#4270=ORIENTED_EDGE('',*,*,#3238,.T.);
#4271=ORIENTED_EDGE('',*,*,#3239,.F.);
#4272=ORIENTED_EDGE('',*,*,#3240,.F.);
#4273=ORIENTED_EDGE('',*,*,#3241,.F.);
#4274=ORIENTED_EDGE('',*,*,#3242,.F.);
#4275=ORIENTED_EDGE('',*,*,#3243,.F.);
#4276=ORIENTED_EDGE('',*,*,#3244,.F.);
#4277=ORIENTED_EDGE('',*,*,#3238,.F.);
#4278=ORIENTED_EDGE('',*,*,#3234,.T.);
#4279=ORIENTED_EDGE('',*,*,#3245,.T.);
#4280=ORIENTED_EDGE('',*,*,#3243,.T.);
#4281=ORIENTED_EDGE('',*,*,#3246,.F.);
#4282=ORIENTED_EDGE('',*,*,#3233,.T.);
#4283=ORIENTED_EDGE('',*,*,#3247,.T.);
#4284=ORIENTED_EDGE('',*,*,#3244,.T.);
#4285=ORIENTED_EDGE('',*,*,#3245,.F.);
#4286=ORIENTED_EDGE('',*,*,#3230,.T.);
#4287=ORIENTED_EDGE('',*,*,#3248,.T.);
#4288=ORIENTED_EDGE('',*,*,#3239,.T.);
#4289=ORIENTED_EDGE('',*,*,#3247,.F.);
#4290=ORIENTED_EDGE('',*,*,#3249,.F.);
#4291=ORIENTED_EDGE('',*,*,#3250,.T.);
#4292=ORIENTED_EDGE('',*,*,#3251,.T.);
#4293=ORIENTED_EDGE('',*,*,#3250,.F.);
#4294=ORIENTED_EDGE('',*,*,#3229,.T.);
#4295=ORIENTED_EDGE('',*,*,#3252,.T.);
#4296=ORIENTED_EDGE('',*,*,#3240,.T.);
#4297=ORIENTED_EDGE('',*,*,#3248,.F.);
#4298=ORIENTED_EDGE('',*,*,#3235,.T.);
#4299=ORIENTED_EDGE('',*,*,#3246,.T.);
#4300=ORIENTED_EDGE('',*,*,#3242,.T.);
#4301=ORIENTED_EDGE('',*,*,#3253,.F.);
#4302=ORIENTED_EDGE('',*,*,#3236,.T.);
#4303=ORIENTED_EDGE('',*,*,#3253,.T.);
#4304=ORIENTED_EDGE('',*,*,#3241,.T.);
#4305=ORIENTED_EDGE('',*,*,#3252,.F.);
#4306=ORIENTED_EDGE('',*,*,#3237,.T.);
#4307=ORIENTED_EDGE('',*,*,#3249,.T.);
#4308=ORIENTED_EDGE('',*,*,#3232,.T.);
#4309=ORIENTED_EDGE('',*,*,#3251,.F.);
#4712=CYLINDRICAL_SURFACE('',#5892,0.2117);
#4959=ADVANCED_FACE('',(#964),#30,.T.);
#4960=ADVANCED_FACE('',(#965),#31,.T.);
#4961=ADVANCED_FACE('',(#966),#677,.T.);
#4962=ADVANCED_FACE('',(#967),#678,.T.);
#4963=ADVANCED_FACE('',(#968),#679,.T.);
#4964=ADVANCED_FACE('',(#969),#4712,.F.);
#4965=ADVANCED_FACE('',(#970),#680,.T.);
#4966=ADVANCED_FACE('',(#971),#681,.T.);
#4967=ADVANCED_FACE('',(#972),#682,.T.);
#4968=ADVANCED_FACE('',(#973,#527),#683,.T.);
#4969=ADVANCED_FACE('',(#974,#528),#684,.F.);
#5070=CLOSED_SHELL('',(#4959,#4960,#4961,#4962,#4963,#4964,#4965,#4966,
#4967,#4968,#4969));
#5884=AXIS2_PLACEMENT_3D('',#9656,#7218,#7219);
#5885=AXIS2_PLACEMENT_3D('',#9657,#7220,#7221);
#5886=AXIS2_PLACEMENT_3D('',#9669,#7223,#7224);
#5887=AXIS2_PLACEMENT_3D('',#9685,#7225,#7226);
#5888=AXIS2_PLACEMENT_3D('',#9687,#7227,#7228);
#5889=AXIS2_PLACEMENT_3D('',#9713,#7230,#7231);
#5890=AXIS2_PLACEMENT_3D('',#9716,#7234,#7235);
#5891=AXIS2_PLACEMENT_3D('',#9718,#7237,#7238);
#5892=AXIS2_PLACEMENT_3D('',#9720,#7240,#7241);
#5893=AXIS2_PLACEMENT_3D('',#9722,#7242,#7243);
#5894=AXIS2_PLACEMENT_3D('',#9725,#7245,#7246);
#5895=AXIS2_PLACEMENT_3D('',#9726,#7247,#7248);
#5896=AXIS2_PLACEMENT_3D('',#9728,#7250,#7251);
#5897=AXIS2_PLACEMENT_3D('',#9730,#7253,#7254);
#5898=AXIS2_PLACEMENT_3D('',#9731,#7255,#7256);
#5899=AXIS2_PLACEMENT_3D('',#9732,#7257,#7258);
#7218=DIRECTION('axis',(0.,0.,1.));
#7219=DIRECTION('refdir',(1.,0.,0.));
#7220=DIRECTION('center_axis',(0.,1.,0.));
#7221=DIRECTION('ref_axis',(1.,0.,0.));
#7222=DIRECTION('',(0.866025403784439,-0.5,1.06057523872491E-16));
#7223=DIRECTION('center_axis',(0.,-1.,0.));
#7224=DIRECTION('ref_axis',(1.,0.,0.));
#7225=DIRECTION('center_axis',(0.,-1.,0.));
#7226=DIRECTION('ref_axis',(1.,0.,0.));
#7227=DIRECTION('center_axis',(0.,1.,0.));
#7228=DIRECTION('ref_axis',(1.,0.,0.));
#7229=DIRECTION('',(-0.866025403784439,-0.5,-1.06057523872491E-16));
#7230=DIRECTION('center_axis',(1.20185167898973E-16,0.,-1.));
#7231=DIRECTION('ref_axis',(-1.,0.,-1.20185167898973E-16));
#7232=DIRECTION('',(0.,1.,0.));
#7233=DIRECTION('',(0.,1.,0.));
#7234=DIRECTION('center_axis',(-0.866025403784439,0.,-0.5));
#7235=DIRECTION('ref_axis',(-0.5,0.,0.866025403784439));
#7236=DIRECTION('',(0.,1.,0.));
#7237=DIRECTION('center_axis',(-0.866025403784439,0.,0.5));
#7238=DIRECTION('ref_axis',(0.5,0.,0.866025403784439));
#7239=DIRECTION('',(0.,1.,0.));
#7240=DIRECTION('center_axis',(0.,1.,0.));
#7241=DIRECTION('ref_axis',(1.,0.,0.));
#7242=DIRECTION('center_axis',(0.,1.,0.));
#7243=DIRECTION('ref_axis',(1.,0.,0.));
#7244=DIRECTION('',(0.,-1.,0.));
#7245=DIRECTION('center_axis',(0.,1.,0.));
#7246=DIRECTION('ref_axis',(1.,0.,0.));
#7247=DIRECTION('center_axis',(-2.40370335797945E-16,0.,1.));
#7248=DIRECTION('ref_axis',(1.,0.,2.40370335797945E-16));
#7249=DIRECTION('',(0.,1.,0.));
#7250=DIRECTION('center_axis',(0.866025403784439,0.,-0.5));
#7251=DIRECTION('ref_axis',(-0.5,0.,-0.866025403784439));
#7252=DIRECTION('',(0.,1.,0.));
#7253=DIRECTION('center_axis',(0.866025403784439,0.,0.5));
#7254=DIRECTION('ref_axis',(0.5,0.,-0.866025403784439));
#7255=DIRECTION('center_axis',(0.,1.,0.));
#7256=DIRECTION('ref_axis',(1.,0.,0.));
#7257=DIRECTION('center_axis',(0.,1.,0.));
#7258=DIRECTION('ref_axis',(1.,0.,0.));
#9656=CARTESIAN_POINT('',(0.,0.,0.));
#9657=CARTESIAN_POINT('Origin',(0.,0.0525042956467857,0.));
#9658=CARTESIAN_POINT('',(-0.230940107675851,0.0472735643746089,0.4));
#9659=CARTESIAN_POINT('',(0.23094010767585,0.0472735643746089,0.4));
#9660=CARTESIAN_POINT('Ctrl Pts',(-0.230940107675851,0.0472735643746089,
0.4));
#9661=CARTESIAN_POINT('Ctrl Pts',(1.11022302462516E-16,-0.0193931022920578,
0.4));
#9662=CARTESIAN_POINT('Ctrl Pts',(0.23094010767585,0.0472735643746089,0.4));
#9663=CARTESIAN_POINT('',(-0.461880215351701,0.0472735643746089,-5.6564012731995E-17));
#9664=CARTESIAN_POINT('Ctrl Pts',(-0.461880215351701,0.0472735643746089,
-5.6564012731995E-17));
#9665=CARTESIAN_POINT('Ctrl Pts',(-0.346410161513776,-0.0193931022920579,
0.2));
#9666=CARTESIAN_POINT('Ctrl Pts',(-0.230940107675851,0.0472735643746089,
0.4));
#9667=CARTESIAN_POINT('',(-0.38,-2.08166817117217E-17,-4.65365783675994E-17));
#9668=CARTESIAN_POINT('',(-0.47094010767585,0.0525042956467857,-5.7673529545534E-17));
#9669=CARTESIAN_POINT('Origin',(0.,0.,0.));
#9670=CARTESIAN_POINT('',(-0.23094010767585,0.0472735643746089,-0.4));
#9671=CARTESIAN_POINT('Ctrl Pts',(-0.23094010767585,0.0472735643746089,
-0.4));
#9672=CARTESIAN_POINT('Ctrl Pts',(-0.346410161513775,-0.0193931022920578,
-0.2));
#9673=CARTESIAN_POINT('Ctrl Pts',(-0.461880215351701,0.0472735643746089,
-5.6564012731995E-17));
#9674=CARTESIAN_POINT('',(0.23094010767585,0.0472735643746089,-0.4));
#9675=CARTESIAN_POINT('Ctrl Pts',(0.23094010767585,0.0472735643746089,-0.4));
#9676=CARTESIAN_POINT('Ctrl Pts',(0.,-0.0193931022920578,-0.4));
#9677=CARTESIAN_POINT('Ctrl Pts',(-0.23094010767585,0.0472735643746089,
-0.4));
#9678=CARTESIAN_POINT('',(0.461880215351701,0.0472735643746089,0.));
#9679=CARTESIAN_POINT('Ctrl Pts',(0.461880215351701,0.0472735643746089,
0.));
#9680=CARTESIAN_POINT('Ctrl Pts',(0.346410161513776,-0.019393102292058,
-0.2));
#9681=CARTESIAN_POINT('Ctrl Pts',(0.23094010767585,0.0472735643746089,-0.4));
#9682=CARTESIAN_POINT('Ctrl Pts',(0.23094010767585,0.0472735643746089,0.4));
#9683=CARTESIAN_POINT('Ctrl Pts',(0.346410161513776,-0.0193931022920577,
0.2));
#9684=CARTESIAN_POINT('Ctrl Pts',(0.461880215351701,0.0472735643746089,
0.));
#9685=CARTESIAN_POINT('Origin',(0.,0.417495704353214,0.));
#9686=CARTESIAN_POINT('',(-0.38,0.47,-4.65365783675994E-17));
#9687=CARTESIAN_POINT('Origin',(0.,0.47,0.));
#9688=CARTESIAN_POINT('',(-0.461880215351701,0.422726435625391,-5.6564012731995E-17));
#9689=CARTESIAN_POINT('',(-0.47094010767585,0.417495704353214,-5.7673529545534E-17));
#9690=CARTESIAN_POINT('',(-0.230940107675851,0.422726435625391,0.4));
#9691=CARTESIAN_POINT('Ctrl Pts',(-0.230940107675851,0.422726435625391,
0.4));
#9692=CARTESIAN_POINT('Ctrl Pts',(-0.346410161513776,0.489393102292058,
0.2));
#9693=CARTESIAN_POINT('Ctrl Pts',(-0.461880215351701,0.422726435625391,
-5.6564012731995E-17));
#9694=CARTESIAN_POINT('',(0.23094010767585,0.422726435625391,0.4));
#9695=CARTESIAN_POINT('Ctrl Pts',(0.23094010767585,0.422726435625391,0.4));
#9696=CARTESIAN_POINT('Ctrl Pts',(8.32667268468867E-17,0.489393102292058,
0.4));
#9697=CARTESIAN_POINT('Ctrl Pts',(-0.230940107675851,0.422726435625391,
0.4));
#9698=CARTESIAN_POINT('',(0.461880215351701,0.422726435625391,0.));
#9699=CARTESIAN_POINT('Ctrl Pts',(0.461880215351701,0.422726435625391,0.));
#9700=CARTESIAN_POINT('Ctrl Pts',(0.346410161513776,0.489393102292058,0.2));
#9701=CARTESIAN_POINT('Ctrl Pts',(0.23094010767585,0.422726435625391,0.4));
#9702=CARTESIAN_POINT('',(0.23094010767585,0.422726435625391,-0.4));
#9703=CARTESIAN_POINT('Ctrl Pts',(0.23094010767585,0.422726435625391,-0.4));
#9704=CARTESIAN_POINT('Ctrl Pts',(0.346410161513775,0.489393102292058,-0.2));
#9705=CARTESIAN_POINT('Ctrl Pts',(0.461880215351701,0.422726435625391,0.));
#9706=CARTESIAN_POINT('',(-0.23094010767585,0.422726435625391,-0.4));
#9707=CARTESIAN_POINT('Ctrl Pts',(-0.23094010767585,0.422726435625391,-0.4));
#9708=CARTESIAN_POINT('Ctrl Pts',(-5.55111512312578E-17,0.489393102292058,
-0.4));
#9709=CARTESIAN_POINT('Ctrl Pts',(0.23094010767585,0.422726435625391,-0.4));
#9710=CARTESIAN_POINT('Ctrl Pts',(-0.461880215351701,0.422726435625391,
-5.6564012731995E-17));
#9711=CARTESIAN_POINT('Ctrl Pts',(-0.346410161513776,0.489393102292058,
-0.2));
#9712=CARTESIAN_POINT('Ctrl Pts',(-0.23094010767585,0.422726435625391,-0.4));
#9713=CARTESIAN_POINT('Origin',(0.23094010767585,0.,-0.4));
#9714=CARTESIAN_POINT('',(-0.23094010767585,0.,-0.4));
#9715=CARTESIAN_POINT('',(0.23094010767585,0.,-0.4));
#9716=CARTESIAN_POINT('Origin',(-0.23094010767585,0.,-0.4));
#9717=CARTESIAN_POINT('',(-0.461880215351701,0.,-5.6564012731995E-17));
#9718=CARTESIAN_POINT('Origin',(-0.461880215351701,0.,-5.6564012731995E-17));
#9719=CARTESIAN_POINT('',(-0.230940107675851,0.,0.4));
#9720=CARTESIAN_POINT('Origin',(0.,0.,0.));
#9721=CARTESIAN_POINT('',(-0.2117,0.47,2.59257727379495E-17));
#9722=CARTESIAN_POINT('Origin',(0.,0.47,0.));
#9723=CARTESIAN_POINT('',(-0.2117,0.,2.59257727379495E-17));
#9724=CARTESIAN_POINT('',(-0.2117,0.,2.59257727379495E-17));
#9725=CARTESIAN_POINT('Origin',(0.,0.,0.));
#9726=CARTESIAN_POINT('Origin',(-0.230940107675851,0.,0.4));
#9727=CARTESIAN_POINT('',(0.23094010767585,0.,0.4));
#9728=CARTESIAN_POINT('Origin',(0.461880215351701,0.,0.));
#9729=CARTESIAN_POINT('',(0.461880215351701,0.,0.));
#9730=CARTESIAN_POINT('Origin',(0.23094010767585,0.,0.4));
#9731=CARTESIAN_POINT('Origin',(0.,0.47,0.));
#9732=CARTESIAN_POINT('Origin',(0.,0.,0.));
#10218=UNCERTAINTY_MEASURE_WITH_UNIT(LENGTH_MEASURE(0.001),#10266,
'DISTANCE_ACCURACY_VALUE',
'Maximum model space distance between geometric entities at asserted c
onnectivities');
#10227=UNCERTAINTY_MEASURE_WITH_UNIT(LENGTH_MEASURE(0.001),#10266,
'DISTANCE_ACCURACY_VALUE',
'Maximum model space distance between geometric entities at asserted c
onnectivities');
#10256=(
GEOMETRIC_REPRESENTATION_CONTEXT(3)
GLOBAL_UNCERTAINTY_ASSIGNED_CONTEXT((#10218))
GLOBAL_UNIT_ASSIGNED_CONTEXT((#10266,#10268,#10269))
REPRESENTATION_CONTEXT('','3D')
);
#10265=(
GEOMETRIC_REPRESENTATION_CONTEXT(3)
GLOBAL_UNCERTAINTY_ASSIGNED_CONTEXT((#10227))
GLOBAL_UNIT_ASSIGNED_CONTEXT((#10266,#10268,#10269))
REPRESENTATION_CONTEXT('','3D')
);
#10266=(
LENGTH_UNIT()
NAMED_UNIT(*)
SI_UNIT(.CENTI.,.METRE.)
);
#10268=(
NAMED_UNIT(*)
PLANE_ANGLE_UNIT()
SI_UNIT($,.RADIAN.)
);
#10269=(
NAMED_UNIT(*)
SI_UNIT($,.STERADIAN.)
SOLID_ANGLE_UNIT()
);
#10298=SHAPE_DEFINITION_REPRESENTATION(#10339,#10432);
#10339=PRODUCT_DEFINITION_SHAPE('',$,#10470);
#10432=SHAPE_REPRESENTATION('',(#5884),#10256);
#10441=PRODUCT_DEFINITION_CONTEXT('part definition',#10554,'design');
#10470=PRODUCT_DEFINITION('Hex Nut - M5','Hex Nut - M5',#10507,#10441);
#10507=PRODUCT_DEFINITION_FORMATION('',$,#10584);
#10554=APPLICATION_CONTEXT(
'Core Data for Automotive Mechanical Design Process');
#10555=PRODUCT_CONTEXT('part definition',#10554,'mechanical');
#10584=PRODUCT('Hex Nut - M5','Hex Nut - M5','Hex Nut - M5',(#10555));
#10656=COLOUR_RGB('Black',0.12,0.14,0.17);
#10657=FILL_AREA_STYLE_COLOUR('',#10656);
#10658=FILL_AREA_STYLE('',(#10657));
#10659=SURFACE_STYLE_FILL_AREA(#10658);
#10660=SURFACE_SIDE_STYLE('',(#10659));
#10661=SURFACE_STYLE_USAGE(.BOTH.,#10660);
#10662=PRESENTATION_STYLE_ASSIGNMENT((#10661));
ENDSEC;
END-ISO-10303-21;
